ISO-10303-21;
HEADER;
/* Generated by software containing ST-Developer
 * from STEP Tools, Inc. (www.steptools.com) 
 */

FILE_DESCRIPTION(
/* description */ ('PAT-080'),
/* implementation_level */ '2;1');

FILE_NAME(
/* name */ 'Cap Screw - M5x20.step',
/* time_stamp */ '2026-10-29T20:13:47-07:00',
/* author */ (''),
/* organization */ (''),
/* preprocessor_version */ 'ST-DEVELOPER v20.2',
/* originating_system */ 'Autodesk Translation Framework v15.17.0.0',
/* authorisation */ '');

FILE_SCHEMA (('AUTOMOTIVE_DESIGN { 1 0 10303 214 3 1 1 }'));
ENDSEC;

DATA;
#10=MECHANICAL_DESIGN_GEOMETRIC_PRESENTATION_REPRESENTATION('',(#259),#6878);
#190=CONICAL_SURFACE('',#4356,0.4,0.785398163397448);
#191=CONICAL_SURFACE('',#4360,0.41,0.785398163397448);
#192=CONICAL_SURFACE('',#4364,0.26,0.463647609000806);
#193=CONICAL_SURFACE('',#4368,0.225,0.785398163397448);
#203=ORIENTED_CLOSED_SHELL('',*,#3877,.F.);
#206=BREP_WITH_VOIDS('Body1',#3876,(#203));
#221=SHAPE_REPRESENTATION_RELATIONSHIP('SRR','None',#6977,#240);
#240=ADVANCED_BREP_SHAPE_REPRESENTATION('',(#206),#6872);
#259=STYLED_ITEM('',(#7136),#206);
#340=FACE_BOUND('',#936,.T.);
#452=PLANE('',#4354);
#453=PLANE('',#4362);
#454=PLANE('',#4370);
#455=PLANE('',#4371);
#456=PLANE('',#4372);
#457=PLANE('',#4373);
#458=PLANE('',#4374);
#459=PLANE('',#4375);
#460=PLANE('',#4376);
#461=PLANE('',#4377);
#462=PLANE('',#4378);
#646=FACE_OUTER_BOUND('',#931,.T.);
#647=FACE_OUTER_BOUND('',#932,.T.);
#648=FACE_OUTER_BOUND('',#933,.T.);
#649=FACE_OUTER_BOUND('',#934,.T.);
#650=FACE_OUTER_BOUND('',#935,.T.);
#651=FACE_OUTER_BOUND('',#937,.T.);
#652=FACE_OUTER_BOUND('',#938,.T.);
#653=FACE_OUTER_BOUND('',#939,.T.);
#654=FACE_OUTER_BOUND('',#940,.T.);
#655=FACE_OUTER_BOUND('',#941,.T.);
#656=FACE_OUTER_BOUND('',#942,.T.);
#657=FACE_OUTER_BOUND('',#943,.T.);
#658=FACE_OUTER_BOUND('',#944,.T.);
#659=FACE_OUTER_BOUND('',#945,.T.);
#660=FACE_OUTER_BOUND('',#946,.T.);
#661=FACE_OUTER_BOUND('',#947,.T.);
#662=FACE_OUTER_BOUND('',#948,.T.);
#931=EDGE_LOOP('',(#3256));
#932=EDGE_LOOP('',(#3257,#3258,#3259,#3260));
#933=EDGE_LOOP('',(#3261,#3262,#3263,#3264));
#934=EDGE_LOOP('',(#3265,#3266,#3267,#3268));
#935=EDGE_LOOP('',(#3269));
#936=EDGE_LOOP('',(#3270));
#937=EDGE_LOOP('',(#3271,#3272,#3273,#3274));
#938=EDGE_LOOP('',(#3275,#3276,#3277,#3278));
#939=EDGE_LOOP('',(#3279,#3280,#3281,#3282));
#940=EDGE_LOOP('',(#3283));
#941=EDGE_LOOP('',(#3284,#3285,#3286,#3287));
#942=EDGE_LOOP('',(#3288,#3289,#3290,#3291));
#943=EDGE_LOOP('',(#3292,#3293,#3294,#3295));
#944=EDGE_LOOP('',(#3296,#3297,#3298,#3299));
#945=EDGE_LOOP('',(#3300,#3301,#3302,#3303));
#946=EDGE_LOOP('',(#3304,#3305,#3306,#3307));
#947=EDGE_LOOP('',(#3308,#3309,#3310,#3311,#3312,#3313));
#948=EDGE_LOOP('',(#3314,#3315,#3316,#3317,#3318,#3319));
#1253=LINE('',#6435,#1568);
#1254=LINE('',#6439,#1569);
#1255=LINE('',#6443,#1570);
#1256=LINE('',#6450,#1571);
#1257=LINE('',#6454,#1572);
#1258=LINE('',#6458,#1573);
#1259=LINE('',#6463,#1574);
#1260=LINE('',#6465,#1575);
#1261=LINE('',#6467,#1576);
#1262=LINE('',#6468,#1577);
#1263=LINE('',#6471,#1578);
#1264=LINE('',#6473,#1579);
#1265=LINE('',#6474,#1580);
#1266=LINE('',#6477,#1581);
#1267=LINE('',#6479,#1582);
#1268=LINE('',#6480,#1583);
#1269=LINE('',#6483,#1584);
#1270=LINE('',#6485,#1585);
#1271=LINE('',#6486,#1586);
#1272=LINE('',#6489,#1587);
#1273=LINE('',#6491,#1588);
#1274=LINE('',#6492,#1589);
#1275=LINE('',#6494,#1590);
#1276=LINE('',#6495,#1591);
#1568=VECTOR('',#5287,0.4);
#1569=VECTOR('',#5292,0.425);
#1570=VECTOR('',#5297,0.41);
#1571=VECTOR('',#5306,0.26);
#1572=VECTOR('',#5311,0.25);
#1573=VECTOR('',#5316,0.225);
#1574=VECTOR('',#5321,1.);
#1575=VECTOR('',#5322,1.);
#1576=VECTOR('',#5323,1.);
#1577=VECTOR('',#5324,1.);
#1578=VECTOR('',#5327,1.);
#1579=VECTOR('',#5328,1.);
#1580=VECTOR('',#5329,1.);
#1581=VECTOR('',#5332,1.);
#1582=VECTOR('',#5333,1.);
#1583=VECTOR('',#5334,1.);
#1584=VECTOR('',#5337,1.);
#1585=VECTOR('',#5338,1.);
#1586=VECTOR('',#5339,1.);
#1587=VECTOR('',#5342,1.);
#1588=VECTOR('',#5343,1.);
#1589=VECTOR('',#5344,1.);
#1590=VECTOR('',#5347,1.);
#1591=VECTOR('',#5348,1.);
#1757=CIRCLE('',#4355,0.375);
#1758=CIRCLE('',#4357,0.425);
#1759=CIRCLE('',#4359,0.425);
#1760=CIRCLE('',#4361,0.395);
#1761=CIRCLE('',#4363,0.27);
#1762=CIRCLE('',#4365,0.24505);
#1763=CIRCLE('',#4367,0.24505);
#1764=CIRCLE('',#4369,0.2);
#2025=VERTEX_POINT('',#6430);
#2026=VERTEX_POINT('',#6433);
#2027=VERTEX_POINT('',#6437);
#2028=VERTEX_POINT('',#6441);
#2029=VERTEX_POINT('',#6445);
#2030=VERTEX_POINT('',#6448);
#2031=VERTEX_POINT('',#6452);
#2032=VERTEX_POINT('',#6456);
#2033=VERTEX_POINT('',#6461);
#2034=VERTEX_POINT('',#6462);
#2035=VERTEX_POINT('',#6464);
#2036=VERTEX_POINT('',#6466);
#2037=VERTEX_POINT('',#6470);
#2038=VERTEX_POINT('',#6472);
#2039=VERTEX_POINT('',#6476);
#2040=VERTEX_POINT('',#6478);
#2041=VERTEX_POINT('',#6482);
#2042=VERTEX_POINT('',#6484);
#2043=VERTEX_POINT('',#6488);
#2044=VERTEX_POINT('',#6490);
#2451=EDGE_CURVE('',#2025,#2025,#1757,.T.);
#2452=EDGE_CURVE('',#2026,#2026,#1758,.T.);
#2453=EDGE_CURVE('',#2026,#2025,#1253,.T.);
#2454=EDGE_CURVE('',#2027,#2027,#1759,.T.);
#2455=EDGE_CURVE('',#2027,#2026,#1254,.T.);
#2456=EDGE_CURVE('',#2028,#2028,#1760,.T.);
#2457=EDGE_CURVE('',#2028,#2027,#1255,.T.);
#2458=EDGE_CURVE('',#2029,#2029,#1761,.T.);
#2459=EDGE_CURVE('',#2030,#2030,#1762,.F.);
#2460=EDGE_CURVE('',#2030,#2029,#1256,.T.);
#2461=EDGE_CURVE('',#2031,#2031,#1763,.F.);
#2462=EDGE_CURVE('',#2031,#2030,#1257,.T.);
#2463=EDGE_CURVE('',#2032,#2032,#1764,.T.);
#2464=EDGE_CURVE('',#2032,#2031,#1258,.T.);
#2465=EDGE_CURVE('',#2033,#2034,#1259,.T.);
#2466=EDGE_CURVE('',#2034,#2035,#1260,.T.);
#2467=EDGE_CURVE('',#2035,#2036,#1261,.T.);
#2468=EDGE_CURVE('',#2033,#2036,#1262,.T.);
#2469=EDGE_CURVE('',#2034,#2037,#1263,.T.);
#2470=EDGE_CURVE('',#2037,#2038,#1264,.T.);
#2471=EDGE_CURVE('',#2038,#2035,#1265,.T.);
#2472=EDGE_CURVE('',#2037,#2039,#1266,.T.);
#2473=EDGE_CURVE('',#2039,#2040,#1267,.T.);
#2474=EDGE_CURVE('',#2040,#2038,#1268,.T.);
#2475=EDGE_CURVE('',#2039,#2041,#1269,.T.);
#2476=EDGE_CURVE('',#2041,#2042,#1270,.T.);
#2477=EDGE_CURVE('',#2042,#2040,#1271,.T.);
#2478=EDGE_CURVE('',#2041,#2043,#1272,.T.);
#2479=EDGE_CURVE('',#2043,#2044,#1273,.T.);
#2480=EDGE_CURVE('',#2044,#2042,#1274,.T.);
#2481=EDGE_CURVE('',#2043,#2033,#1275,.T.);
#2482=EDGE_CURVE('',#2036,#2044,#1276,.T.);
#3256=ORIENTED_EDGE('',*,*,#2451,.F.);
#3257=ORIENTED_EDGE('',*,*,#2452,.F.);
#3258=ORIENTED_EDGE('',*,*,#2453,.T.);
#3259=ORIENTED_EDGE('',*,*,#2451,.T.);
#3260=ORIENTED_EDGE('',*,*,#2453,.F.);
#3261=ORIENTED_EDGE('',*,*,#2454,.F.);
#3262=ORIENTED_EDGE('',*,*,#2455,.T.);
#3263=ORIENTED_EDGE('',*,*,#2452,.T.);
#3264=ORIENTED_EDGE('',*,*,#2455,.F.);
#3265=ORIENTED_EDGE('',*,*,#2456,.F.);
#3266=ORIENTED_EDGE('',*,*,#2457,.T.);
#3267=ORIENTED_EDGE('',*,*,#2454,.T.);
#3268=ORIENTED_EDGE('',*,*,#2457,.F.);
#3269=ORIENTED_EDGE('',*,*,#2456,.T.);
#3270=ORIENTED_EDGE('',*,*,#2458,.F.);
#3271=ORIENTED_EDGE('',*,*,#2459,.F.);
#3272=ORIENTED_EDGE('',*,*,#2460,.T.);
#3273=ORIENTED_EDGE('',*,*,#2458,.T.);
#3274=ORIENTED_EDGE('',*,*,#2460,.F.);
#3275=ORIENTED_EDGE('',*,*,#2461,.F.);
#3276=ORIENTED_EDGE('',*,*,#2462,.T.);
#3277=ORIENTED_EDGE('',*,*,#2459,.T.);
#3278=ORIENTED_EDGE('',*,*,#2462,.F.);
#3279=ORIENTED_EDGE('',*,*,#2463,.F.);
#3280=ORIENTED_EDGE('',*,*,#2464,.T.);
#3281=ORIENTED_EDGE('',*,*,#2461,.T.);
#3282=ORIENTED_EDGE('',*,*,#2464,.F.);
#3283=ORIENTED_EDGE('',*,*,#2463,.T.);
#3284=ORIENTED_EDGE('',*,*,#2465,.T.);
#3285=ORIENTED_EDGE('',*,*,#2466,.T.);
#3286=ORIENTED_EDGE('',*,*,#2467,.T.);
#3287=ORIENTED_EDGE('',*,*,#2468,.F.);
#3288=ORIENTED_EDGE('',*,*,#2469,.T.);
#3289=ORIENTED_EDGE('',*,*,#2470,.T.);
#3290=ORIENTED_EDGE('',*,*,#2471,.T.);
#3291=ORIENTED_EDGE('',*,*,#2466,.F.);
#3292=ORIENTED_EDGE('',*,*,#2472,.T.);
#3293=ORIENTED_EDGE('',*,*,#2473,.T.);
#3294=ORIENTED_EDGE('',*,*,#2474,.T.);
#3295=ORIENTED_EDGE('',*,*,#2470,.F.);
#3296=ORIENTED_EDGE('',*,*,#2475,.T.);
#3297=ORIENTED_EDGE('',*,*,#2476,.T.);
#3298=ORIENTED_EDGE('',*,*,#2477,.T.);
#3299=ORIENTED_EDGE('',*,*,#2473,.F.);
#3300=ORIENTED_EDGE('',*,*,#2478,.T.);
#3301=ORIENTED_EDGE('',*,*,#2479,.T.);
#3302=ORIENTED_EDGE('',*,*,#2480,.T.);
#3303=ORIENTED_EDGE('',*,*,#2476,.F.);
#3304=ORIENTED_EDGE('',*,*,#2481,.T.);
#3305=ORIENTED_EDGE('',*,*,#2468,.T.);
#3306=ORIENTED_EDGE('',*,*,#2482,.T.);
#3307=ORIENTED_EDGE('',*,*,#2479,.F.);
#3308=ORIENTED_EDGE('',*,*,#2481,.F.);
#3309=ORIENTED_EDGE('',*,*,#2478,.F.);
#3310=ORIENTED_EDGE('',*,*,#2475,.F.);
#3311=ORIENTED_EDGE('',*,*,#2472,.F.);
#3312=ORIENTED_EDGE('',*,*,#2469,.F.);
#3313=ORIENTED_EDGE('',*,*,#2465,.F.);
#3314=ORIENTED_EDGE('',*,*,#2482,.F.);
#3315=ORIENTED_EDGE('',*,*,#2467,.F.);
#3316=ORIENTED_EDGE('',*,*,#2471,.F.);
#3317=ORIENTED_EDGE('',*,*,#2474,.F.);
#3318=ORIENTED_EDGE('',*,*,#2477,.F.);
#3319=ORIENTED_EDGE('',*,*,#2480,.F.);
#3618=CYLINDRICAL_SURFACE('',#4358,0.425);
#3619=CYLINDRICAL_SURFACE('',#4366,0.24505);
#3782=ADVANCED_FACE('',(#646),#452,.T.);
#3783=ADVANCED_FACE('',(#647),#190,.T.);
#3784=ADVANCED_FACE('',(#648),#3618,.T.);
#3785=ADVANCED_FACE('',(#649),#191,.T.);
#3786=ADVANCED_FACE('',(#650,#340),#453,.T.);
#3787=ADVANCED_FACE('',(#651),#192,.T.);
#3788=ADVANCED_FACE('',(#652),#3619,.T.);
#3789=ADVANCED_FACE('',(#653),#193,.T.);
#3790=ADVANCED_FACE('',(#654),#454,.T.);
#3791=ADVANCED_FACE('',(#655),#455,.F.);
#3792=ADVANCED_FACE('',(#656),#456,.F.);
#3793=ADVANCED_FACE('',(#657),#457,.F.);
#3794=ADVANCED_FACE('',(#658),#458,.F.);
#3795=ADVANCED_FACE('',(#659),#459,.F.);
#3796=ADVANCED_FACE('',(#660),#460,.F.);
#3797=ADVANCED_FACE('',(#661),#461,.F.);
#3798=ADVANCED_FACE('',(#662),#462,.F.);
#3876=CLOSED_SHELL('',(#3782,#3783,#3784,#3785,#3786,#3787,#3788,#3789,
#3790));
#3877=CLOSED_SHELL('',(#3791,#3792,#3793,#3794,#3795,#3796,#3797,#3798));
#4353=AXIS2_PLACEMENT_3D('',#6428,#5277,#5278);
#4354=AXIS2_PLACEMENT_3D('',#6429,#5279,#5280);
#4355=AXIS2_PLACEMENT_3D('',#6431,#5281,#5282);
#4356=AXIS2_PLACEMENT_3D('',#6432,#5283,#5284);
#4357=AXIS2_PLACEMENT_3D('',#6434,#5285,#5286);
#4358=AXIS2_PLACEMENT_3D('',#6436,#5288,#5289);
#4359=AXIS2_PLACEMENT_3D('',#6438,#5290,#5291);
#4360=AXIS2_PLACEMENT_3D('',#6440,#5293,#5294);
#4361=AXIS2_PLACEMENT_3D('',#6442,#5295,#5296);
#4362=AXIS2_PLACEMENT_3D('',#6444,#5298,#5299);
#4363=AXIS2_PLACEMENT_3D('',#6446,#5300,#5301);
#4364=AXIS2_PLACEMENT_3D('',#6447,#5302,#5303);
#4365=AXIS2_PLACEMENT_3D('',#6449,#5304,#5305);
#4366=AXIS2_PLACEMENT_3D('',#6451,#5307,#5308);
#4367=AXIS2_PLACEMENT_3D('',#6453,#5309,#5310);
#4368=AXIS2_PLACEMENT_3D('',#6455,#5312,#5313);
#4369=AXIS2_PLACEMENT_3D('',#6457,#5314,#5315);
#4370=AXIS2_PLACEMENT_3D('',#6459,#5317,#5318);
#4371=AXIS2_PLACEMENT_3D('',#6460,#5319,#5320);
#4372=AXIS2_PLACEMENT_3D('',#6469,#5325,#5326);
#4373=AXIS2_PLACEMENT_3D('',#6475,#5330,#5331);
#4374=AXIS2_PLACEMENT_3D('',#6481,#5335,#5336);
#4375=AXIS2_PLACEMENT_3D('',#6487,#5340,#5341);
#4376=AXIS2_PLACEMENT_3D('',#6493,#5345,#5346);
#4377=AXIS2_PLACEMENT_3D('',#6496,#5349,#5350);
#4378=AXIS2_PLACEMENT_3D('',#6497,#5351,#5352);
#5277=DIRECTION('axis',(0.,0.,1.));
#5278=DIRECTION('refdir',(1.,0.,0.));
#5279=DIRECTION('center_axis',(0.,1.,0.));
#5280=DIRECTION('ref_axis',(0.,0.,1.));
#5281=DIRECTION('center_axis',(0.,-1.,0.));
#5282=DIRECTION('ref_axis',(1.,0.,0.));
#5283=DIRECTION('center_axis',(0.,-1.,0.));
#5284=DIRECTION('ref_axis',(1.,0.,0.));
#5285=DIRECTION('center_axis',(0.,-1.,0.));
#5286=DIRECTION('ref_axis',(1.,0.,0.));
#5287=DIRECTION('',(0.707106781186548,0.707106781186547,8.65956056235493E-17));
#5288=DIRECTION('center_axis',(0.,-1.,0.));
#5289=DIRECTION('ref_axis',(1.,0.,0.));
#5290=DIRECTION('center_axis',(0.,-1.,0.));
#5291=DIRECTION('ref_axis',(1.,0.,0.));
#5292=DIRECTION('',(0.,1.,0.));
#5293=DIRECTION('center_axis',(0.,1.,0.));
#5294=DIRECTION('ref_axis',(1.,0.,0.));
#5295=DIRECTION('center_axis',(0.,-1.,0.));
#5296=DIRECTION('ref_axis',(1.,0.,0.));
#5297=DIRECTION('',(-0.707106781186547,0.707106781186548,-8.65956056235493E-17));
#5298=DIRECTION('center_axis',(0.,-1.,0.));
#5299=DIRECTION('ref_axis',(0.,0.,-1.));
#5300=DIRECTION('center_axis',(0.,-1.,0.));
#5301=DIRECTION('ref_axis',(1.,0.,0.));
#5302=DIRECTION('center_axis',(0.,1.,0.));
#5303=DIRECTION('ref_axis',(1.,0.,0.));
#5304=DIRECTION('center_axis',(0.,1.,0.));
#5305=DIRECTION('ref_axis',(1.,0.,0.));
#5306=DIRECTION('',(-0.447213595499958,0.894427190999916,-5.47678698264203E-17));
#5307=DIRECTION('center_axis',(0.,-1.,0.));
#5308=DIRECTION('ref_axis',(1.,0.,0.));
#5309=DIRECTION('center_axis',(0.,1.,0.));
#5310=DIRECTION('ref_axis',(1.,0.,0.));
#5311=DIRECTION('',(0.,1.,0.));
#5312=DIRECTION('center_axis',(0.,1.,0.));
#5313=DIRECTION('ref_axis',(1.,0.,0.));
#5314=DIRECTION('center_axis',(0.,-1.,0.));
#5315=DIRECTION('ref_axis',(1.,0.,0.));
#5316=DIRECTION('',(-0.707106781186547,0.707106781186548,-8.65956056235493E-17));
#5317=DIRECTION('center_axis',(0.,-1.,0.));
#5318=DIRECTION('ref_axis',(0.,0.,-1.));
#5319=DIRECTION('center_axis',(0.866025403784439,0.,-0.5));
#5320=DIRECTION('ref_axis',(0.5,0.,0.866025403784439));
#5321=DIRECTION('',(-0.5,0.,-0.866025403784439));
#5322=DIRECTION('',(0.,-1.,0.));
#5323=DIRECTION('',(0.5,0.,0.866025403784439));
#5324=DIRECTION('',(0.,-1.,0.));
#5325=DIRECTION('center_axis',(1.20185167898973E-16,0.,-1.));
#5326=DIRECTION('ref_axis',(1.,0.,1.20185167898973E-16));
#5327=DIRECTION('',(-1.,0.,-1.20185167898973E-16));
#5328=DIRECTION('',(0.,-1.,0.));
#5329=DIRECTION('',(1.,0.,1.20185167898973E-16));
#5330=DIRECTION('center_axis',(-0.866025403784439,0.,-0.5));
#5331=DIRECTION('ref_axis',(0.5,0.,-0.866025403784439));
#5332=DIRECTION('',(-0.5,0.,0.866025403784439));
#5333=DIRECTION('',(0.,-1.,0.));
#5334=DIRECTION('',(0.5,0.,-0.866025403784439));
#5335=DIRECTION('center_axis',(-0.866025403784439,0.,0.5));
#5336=DIRECTION('ref_axis',(-0.5,0.,-0.866025403784439));
#5337=DIRECTION('',(0.5,0.,0.866025403784439));
#5338=DIRECTION('',(0.,-1.,0.));
#5339=DIRECTION('',(-0.5,0.,-0.866025403784439));
#5340=DIRECTION('center_axis',(-2.40370335797945E-16,0.,1.));
#5341=DIRECTION('ref_axis',(-1.,0.,-2.40370335797945E-16));
#5342=DIRECTION('',(1.,0.,2.40370335797945E-16));
#5343=DIRECTION('',(0.,-1.,0.));
#5344=DIRECTION('',(-1.,0.,-2.40370335797945E-16));
#5345=DIRECTION('center_axis',(0.866025403784439,0.,0.5));
#5346=DIRECTION('ref_axis',(-0.5,0.,0.866025403784439));
#5347=DIRECTION('',(0.5,0.,-0.866025403784439));
#5348=DIRECTION('',(-0.5,0.,0.866025403784439));
#5349=DIRECTION('center_axis',(0.,1.,0.));
#5350=DIRECTION('ref_axis',(1.,0.,0.));
#5351=DIRECTION('center_axis',(0.,-1.,0.));
#5352=DIRECTION('ref_axis',(0.,0.,-1.));
#6428=CARTESIAN_POINT('',(0.,0.,0.));
#6429=CARTESIAN_POINT('Origin',(0.375,0.5,0.));
#6430=CARTESIAN_POINT('',(-0.375,0.5,-4.59242549680257E-17));
#6431=CARTESIAN_POINT('Origin',(0.,0.5,0.));
#6432=CARTESIAN_POINT('Origin',(0.,0.475,0.));
#6433=CARTESIAN_POINT('',(-0.425,0.45,-5.20474889637625E-17));
#6434=CARTESIAN_POINT('Origin',(0.,0.45,0.));
#6435=CARTESIAN_POINT('',(-0.4,0.475,-4.89858719658941E-17));
#6436=CARTESIAN_POINT('Origin',(0.,0.24,0.));
#6437=CARTESIAN_POINT('',(-0.425,0.0299999999999998,-5.20474889637625E-17));
#6438=CARTESIAN_POINT('Origin',(0.,0.0299999999999998,0.));
#6439=CARTESIAN_POINT('',(-0.425,0.24,-5.20474889637625E-17));
#6440=CARTESIAN_POINT('Origin',(0.,0.0150000000000001,0.));
#6441=CARTESIAN_POINT('',(-0.395,4.85722573273506E-17,-4.83735485663204E-17));
#6442=CARTESIAN_POINT('Origin',(0.,0.,0.));
#6443=CARTESIAN_POINT('',(-0.41,0.0150000000000001,-5.02105187650415E-17));
#6444=CARTESIAN_POINT('Origin',(0.27,0.,0.));
#6445=CARTESIAN_POINT('',(-0.27,0.,-3.30654635769785E-17));
#6446=CARTESIAN_POINT('Origin',(0.,0.,0.));
#6447=CARTESIAN_POINT('Origin',(0.,-0.02,0.));
#6448=CARTESIAN_POINT('',(-0.24505,-0.0498999999999999,3.00099698131059E-17));
#6449=CARTESIAN_POINT('Origin',(0.,-0.0498999999999999,0.));
#6450=CARTESIAN_POINT('',(-0.26,-0.02,-3.18408167778312E-17));
#6451=CARTESIAN_POINT('Origin',(0.,-0.995,0.));
#6452=CARTESIAN_POINT('',(-0.24505,-1.95495,3.00099698131059E-17));
#6453=CARTESIAN_POINT('Origin',(0.,-1.95495,0.));
#6454=CARTESIAN_POINT('',(-0.24505,-0.995,-3.00099698131059E-17));
#6455=CARTESIAN_POINT('Origin',(0.,-1.975,0.));
#6456=CARTESIAN_POINT('',(-0.2,-2.,-2.44929359829471E-17));
#6457=CARTESIAN_POINT('Origin',(0.,-2.,0.));
#6458=CARTESIAN_POINT('',(-0.225,-1.975,-2.75545529808154E-17));
#6459=CARTESIAN_POINT('Origin',(0.,-2.,0.));
#6460=CARTESIAN_POINT('Origin',(0.115470053837925,-0.5,-0.2));
#6461=CARTESIAN_POINT('',(0.23094010767585,-0.5,0.));
#6462=CARTESIAN_POINT('',(0.115470053837925,-0.5,-0.2));
#6463=CARTESIAN_POINT('',(0.23094010767585,-0.5,0.));
#6464=CARTESIAN_POINT('',(0.115470053837925,-0.8,-0.2));
#6465=CARTESIAN_POINT('',(0.115470053837925,-0.5,-0.2));
#6466=CARTESIAN_POINT('',(0.23094010767585,-0.8,0.));
#6467=CARTESIAN_POINT('',(0.23094010767585,-0.8,0.));
#6468=CARTESIAN_POINT('',(0.23094010767585,-0.5,0.));
#6469=CARTESIAN_POINT('Origin',(-0.115470053837925,-0.5,-0.2));
#6470=CARTESIAN_POINT('',(-0.115470053837925,-0.5,-0.2));
#6471=CARTESIAN_POINT('',(0.115470053837925,-0.5,-0.2));
#6472=CARTESIAN_POINT('',(-0.115470053837925,-0.8,-0.2));
#6473=CARTESIAN_POINT('',(-0.115470053837925,-0.5,-0.2));
#6474=CARTESIAN_POINT('',(0.115470053837925,-0.8,-0.2));
#6475=CARTESIAN_POINT('Origin',(-0.23094010767585,-0.5,-2.77555756156289E-17));
#6476=CARTESIAN_POINT('',(-0.23094010767585,-0.5,-2.82820063659975E-17));
#6477=CARTESIAN_POINT('',(-0.115470053837925,-0.5,-0.2));
#6478=CARTESIAN_POINT('',(-0.23094010767585,-0.8,-2.77555756156289E-17));
#6479=CARTESIAN_POINT('',(-0.23094010767585,-0.5,-2.82820063659975E-17));
#6480=CARTESIAN_POINT('',(-0.115470053837925,-0.8,-0.2));
#6481=CARTESIAN_POINT('Origin',(-0.115470053837925,-0.5,0.2));
#6482=CARTESIAN_POINT('',(-0.115470053837925,-0.5,0.2));
#6483=CARTESIAN_POINT('',(-0.23094010767585,-0.5,-2.82820063659975E-17));
#6484=CARTESIAN_POINT('',(-0.115470053837925,-0.8,0.2));
#6485=CARTESIAN_POINT('',(-0.115470053837925,-0.5,0.2));
#6486=CARTESIAN_POINT('',(-0.23094010767585,-0.8,-2.82820063659975E-17));
#6487=CARTESIAN_POINT('Origin',(0.115470053837925,-0.5,0.2));
#6488=CARTESIAN_POINT('',(0.115470053837925,-0.5,0.2));
#6489=CARTESIAN_POINT('',(-0.115470053837925,-0.5,0.2));
#6490=CARTESIAN_POINT('',(0.115470053837925,-0.8,0.2));
#6491=CARTESIAN_POINT('',(0.115470053837925,-0.5,0.2));
#6492=CARTESIAN_POINT('',(-0.115470053837925,-0.8,0.2));
#6493=CARTESIAN_POINT('Origin',(0.23094010767585,-0.5,0.));
#6494=CARTESIAN_POINT('',(0.115470053837925,-0.5,0.2));
#6495=CARTESIAN_POINT('',(0.115470053837925,-0.8,0.2));
#6496=CARTESIAN_POINT('Origin',(0.,-0.5,0.));
#6497=CARTESIAN_POINT('Origin',(0.,-0.8,0.));
#6851=UNCERTAINTY_MEASURE_WITH_UNIT(LENGTH_MEASURE(0.001),#6879,
'DISTANCE_ACCURACY_VALUE',
'Maximum model space distance between geometric entities at asserted c
onnectivities');
#6857=UNCERTAINTY_MEASURE_WITH_UNIT(LENGTH_MEASURE(0.001),#6879,
'DISTANCE_ACCURACY_VALUE',
'Maximum model space distance between geometric entities at asserted c
onnectivities');
#6872=(
GEOMETRIC_REPRESENTATION_CONTEXT(3)
GLOBAL_UNCERTAINTY_ASSIGNED_CONTEXT((#6851))
GLOBAL_UNIT_ASSIGNED_CONTEXT((#6879,#6881,#6882))
REPRESENTATION_CONTEXT('','3D')
);
#6878=(
GEOMETRIC_REPRESENTATION_CONTEXT(3)
GLOBAL_UNCERTAINTY_ASSIGNED_CONTEXT((#6857))
GLOBAL_UNIT_ASSIGNED_CONTEXT((#6879,#6881,#6882))
REPRESENTATION_CONTEXT('','3D')
);
#6879=(
LENGTH_UNIT()
NAMED_UNIT(*)
SI_UNIT(.CENTI.,.METRE.)
);
#6881=(
NAMED_UNIT(*)
PLANE_ANGLE_UNIT()
SI_UNIT($,.RADIAN.)
);
#6882=(
NAMED_UNIT(*)
SI_UNIT($,.STERADIAN.)
SOLID_ANGLE_UNIT()
);
#6897=SHAPE_DEFINITION_REPRESENTATION(#6917,#6977);
#6917=PRODUCT_DEFINITION_SHAPE('',$,#6998);
#6977=SHAPE_REPRESENTATION('',(#4353),#6872);
#6983=PRODUCT_DEFINITION_CONTEXT('part definition',#7045,'design');
#6998=PRODUCT_DEFINITION('Cap Screw - M5x20','Cap Screw - M5x20',
#7018,#6983);
#7018=PRODUCT_DEFINITION_FORMATION('',$,#7061);
#7045=APPLICATION_CONTEXT(
'Core Data for Automotive Mechanical Design Process');
#7046=PRODUCT_CONTEXT('part definition',#7045,'mechanical');
#7061=PRODUCT('Cap Screw - M5x20','Cap Screw - M5x20',
'Cap Screw - M5x20',(#7046));
#7130=COLOUR_RGB('Black',0.12,0.14,0.17);
#7131=FILL_AREA_STYLE_COLOUR('',#7130);
#7132=FILL_AREA_STYLE('',(#7131));
#7133=SURFACE_STYLE_FILL_AREA(#7132);
#7134=SURFACE_SIDE_STYLE('',(#7133));
#7135=SURFACE_STYLE_USAGE(.BOTH.,#7134);
#7136=PRESENTATION_STYLE_ASSIGNMENT((#7135));
ENDSEC;
END-ISO-10303-21;
